ISO-10303-21;
HEADER;
/* Generated by software containing ST-Developer
 * from STEP Tools, Inc. (www.steptools.com) 
 */

FILE_DESCRIPTION(
/* description */ ('Double-row support with tensioned shaft'),
/* implementation_level */ '2;1');

FILE_NAME(
/* name */ 'Captive slot nut.step',
/* time_stamp */ '2026-10-27T10:50:35-07:00',
/* author */ (''),
/* organization */ (''),
/* preprocessor_version */ 'ST-DEVELOPER v20.2',
/* originating_system */ 'Autodesk Translation Framework v15.17.0.0',
/* authorisation */ '');

FILE_SCHEMA (('AUTOMOTIVE_DESIGN { 1 0 10303 214 3 1 1 }'));
ENDSEC;

DATA;
#10=MECHANICAL_DESIGN_GEOMETRIC_PRESENTATION_REPRESENTATION('',(#495),#11559);
#413=ELLIPSE('',#6979,0.299389011154384,0.2117);
#414=ELLIPSE('',#6983,0.299389011154384,0.2117);
#431=SHAPE_REPRESENTATION_RELATIONSHIP('SRR','None',#11739,#463);
#463=ADVANCED_BREP_SHAPE_REPRESENTATION('',(#528),#11541);
#495=STYLED_ITEM('',(#11974),#528);
#528=MANIFOLD_SOLID_BREP('Body1',#6340);
#612=FACE_BOUND('',#1485,.T.);
#787=PLANE('',#6969);
#788=PLANE('',#6970);
#789=PLANE('',#6971);
#790=PLANE('',#6973);
#791=PLANE('',#6974);
#792=PLANE('',#6975);
#793=PLANE('',#6976);
#794=PLANE('',#6977);
#795=PLANE('',#6978);
#796=PLANE('',#6985);
#797=PLANE('',#6986);
#798=PLANE('',#6987);
#799=PLANE('',#6988);
#1068=FACE_OUTER_BOUND('',#1482,.T.);
#1069=FACE_OUTER_BOUND('',#1483,.T.);
#1070=FACE_OUTER_BOUND('',#1484,.T.);
#1071=FACE_OUTER_BOUND('',#1486,.T.);
#1072=FACE_OUTER_BOUND('',#1487,.T.);
#1073=FACE_OUTER_BOUND('',#1488,.T.);
#1074=FACE_OUTER_BOUND('',#1489,.T.);
#1075=FACE_OUTER_BOUND('',#1490,.T.);
#1076=FACE_OUTER_BOUND('',#1491,.T.);
#1077=FACE_OUTER_BOUND('',#1492,.T.);
#1078=FACE_OUTER_BOUND('',#1493,.T.);
#1079=FACE_OUTER_BOUND('',#1494,.T.);
#1080=FACE_OUTER_BOUND('',#1495,.T.);
#1081=FACE_OUTER_BOUND('',#1496,.T.);
#1482=EDGE_LOOP('',(#5044,#5045,#5046,#5047));
#1483=EDGE_LOOP('',(#5048,#5049,#5050,#5051));
#1484=EDGE_LOOP('',(#5052,#5053,#5054,#5055));
#1485=EDGE_LOOP('',(#5056));
#1486=EDGE_LOOP('',(#5057,#5058,#5059,#5060,#5061,#5062,#5063,#5064,#5065,
#5066));
#1487=EDGE_LOOP('',(#5067,#5068,#5069,#5070));
#1488=EDGE_LOOP('',(#5071,#5072,#5073,#5074));
#1489=EDGE_LOOP('',(#5075,#5076,#5077,#5078,#5079,#5080,#5081,#5082,#5083,
#5084));
#1490=EDGE_LOOP('',(#5085,#5086,#5087,#5088));
#1491=EDGE_LOOP('',(#5089,#5090,#5091,#5092,#5093,#5094));
#1492=EDGE_LOOP('',(#5095,#5096,#5097,#5098,#5099,#5100,#5101,#5102));
#1493=EDGE_LOOP('',(#5103,#5104,#5105,#5106,#5107));
#1494=EDGE_LOOP('',(#5108,#5109,#5110,#5111));
#1495=EDGE_LOOP('',(#5112,#5113,#5114,#5115,#5116,#5117));
#1496=EDGE_LOOP('',(#5118,#5119,#5120,#5121));
#2013=LINE('',#10002,#2560);
#2014=LINE('',#10004,#2561);
#2015=LINE('',#10006,#2562);
#2016=LINE('',#10007,#2563);
#2017=LINE('',#10010,#2564);
#2018=LINE('',#10012,#2565);
#2019=LINE('',#10013,#2566);
#2020=LINE('',#10016,#2567);
#2021=LINE('',#10018,#2568);
#2022=LINE('',#10019,#2569);
#2023=LINE('',#10024,#2570);
#2024=LINE('',#10026,#2571);
#2025=LINE('',#10028,#2572);
#2026=LINE('',#10030,#2573);
#2027=LINE('',#10032,#2574);
#2028=LINE('',#10034,#2575);
#2029=LINE('',#10035,#2576);
#2030=LINE('',#10038,#2577);
#2031=LINE('',#10039,#2578);
#2032=LINE('',#10042,#2579);
#2033=LINE('',#10043,#2580);
#2034=LINE('',#10046,#2581);
#2035=LINE('',#10048,#2582);
#2036=LINE('',#10050,#2583);
#2037=LINE('',#10052,#2584);
#2038=LINE('',#10053,#2585);
#2039=LINE('',#10055,#2586);
#2040=LINE('',#10058,#2587);
#2041=LINE('',#10061,#2588);
#2042=LINE('',#10065,#2589);
#2043=LINE('',#10072,#2590);
#2044=LINE('',#10074,#2591);
#2045=LINE('',#10076,#2592);
#2560=VECTOR('',#8156,1.);
#2561=VECTOR('',#8157,1.);
#2562=VECTOR('',#8158,1.);
#2563=VECTOR('',#8159,1.);
#2564=VECTOR('',#8162,1.);
#2565=VECTOR('',#8163,1.);
#2566=VECTOR('',#8164,1.);
#2567=VECTOR('',#8167,1.);
#2568=VECTOR('',#8168,1.);
#2569=VECTOR('',#8169,1.);
#2570=VECTOR('',#8174,1.);
#2571=VECTOR('',#8175,1.);
#2572=VECTOR('',#8176,1.);
#2573=VECTOR('',#8177,1.);
#2574=VECTOR('',#8178,1.);
#2575=VECTOR('',#8179,1.);
#2576=VECTOR('',#8180,1.);
#2577=VECTOR('',#8183,1.);
#2578=VECTOR('',#8184,1.);
#2579=VECTOR('',#8187,1.);
#2580=VECTOR('',#8188,1.);
#2581=VECTOR('',#8191,1.);
#2582=VECTOR('',#8192,1.);
#2583=VECTOR('',#8193,1.);
#2584=VECTOR('',#8194,1.);
#2585=VECTOR('',#8195,1.);
#2586=VECTOR('',#8198,1.);
#2587=VECTOR('',#8201,1.);
#2588=VECTOR('',#8204,1.);
#2589=VECTOR('',#8209,0.21);
#2590=VECTOR('',#8218,1.);
#2591=VECTOR('',#8221,1.);
#2592=VECTOR('',#8224,1.);
#2922=CIRCLE('',#6972,0.2117);
#2923=CIRCLE('',#6981,0.2117);
#2924=CIRCLE('',#6982,0.2117);
#2925=CIRCLE('',#6984,0.2117);
#3265=VERTEX_POINT('',#10000);
#3266=VERTEX_POINT('',#10001);
#3267=VERTEX_POINT('',#10003);
#3268=VERTEX_POINT('',#10005);
#3269=VERTEX_POINT('',#10009);
#3270=VERTEX_POINT('',#10011);
#3271=VERTEX_POINT('',#10015);
#3272=VERTEX_POINT('',#10017);
#3273=VERTEX_POINT('',#10020);
#3274=VERTEX_POINT('',#10023);
#3275=VERTEX_POINT('',#10025);
#3276=VERTEX_POINT('',#10027);
#3277=VERTEX_POINT('',#10029);
#3278=VERTEX_POINT('',#10031);
#3279=VERTEX_POINT('',#10033);
#3280=VERTEX_POINT('',#10037);
#3281=VERTEX_POINT('',#10041);
#3282=VERTEX_POINT('',#10045);
#3283=VERTEX_POINT('',#10047);
#3284=VERTEX_POINT('',#10049);
#3285=VERTEX_POINT('',#10051);
#3286=VERTEX_POINT('',#10057);
#3287=VERTEX_POINT('',#10059);
#3288=VERTEX_POINT('',#10063);
#3289=VERTEX_POINT('',#10066);
#3290=VERTEX_POINT('',#10068);
#3907=EDGE_CURVE('',#3265,#3266,#2013,.T.);
#3908=EDGE_CURVE('',#3267,#3265,#2014,.T.);
#3909=EDGE_CURVE('',#3268,#3267,#2015,.T.);
#3910=EDGE_CURVE('',#3266,#3268,#2016,.T.);
#3911=EDGE_CURVE('',#3267,#3269,#2017,.T.);
#3912=EDGE_CURVE('',#3270,#3269,#2018,.T.);
#3913=EDGE_CURVE('',#3268,#3270,#2019,.T.);
#3914=EDGE_CURVE('',#3269,#3271,#2020,.T.);
#3915=EDGE_CURVE('',#3271,#3272,#2021,.T.);
#3916=EDGE_CURVE('',#3272,#3270,#2022,.T.);
#3917=EDGE_CURVE('',#3273,#3273,#2922,.T.);
#3918=EDGE_CURVE('',#3274,#3265,#2023,.T.);
#3919=EDGE_CURVE('',#3275,#3274,#2024,.T.);
#3920=EDGE_CURVE('',#3275,#3276,#2025,.T.);
#3921=EDGE_CURVE('',#3277,#3276,#2026,.T.);
#3922=EDGE_CURVE('',#3277,#3278,#2027,.T.);
#3923=EDGE_CURVE('',#3278,#3279,#2028,.T.);
#3924=EDGE_CURVE('',#3279,#3271,#2029,.T.);
#3925=EDGE_CURVE('',#3279,#3280,#2030,.T.);
#3926=EDGE_CURVE('',#3280,#3272,#2031,.T.);
#3927=EDGE_CURVE('',#3281,#3278,#2032,.T.);
#3928=EDGE_CURVE('',#3280,#3281,#2033,.T.);
#3929=EDGE_CURVE('',#3282,#3281,#2034,.T.);
#3930=EDGE_CURVE('',#3283,#3282,#2035,.T.);
#3931=EDGE_CURVE('',#3283,#3284,#2036,.T.);
#3932=EDGE_CURVE('',#3285,#3284,#2037,.T.);
#3933=EDGE_CURVE('',#3285,#3266,#2038,.T.);
#3934=EDGE_CURVE('',#3282,#3277,#2039,.T.);
#3935=EDGE_CURVE('',#3276,#3286,#2040,.T.);
#3936=EDGE_CURVE('',#3286,#3287,#413,.T.);
#3937=EDGE_CURVE('',#3287,#3283,#2041,.T.);
#3938=EDGE_CURVE('',#3288,#3286,#2923,.F.);
#3939=EDGE_CURVE('',#3288,#3273,#2042,.T.);
#3940=EDGE_CURVE('',#3289,#3288,#2924,.F.);
#3941=EDGE_CURVE('',#3290,#3289,#414,.T.);
#3942=EDGE_CURVE('',#3287,#3290,#2925,.F.);
#3943=EDGE_CURVE('',#3289,#3275,#2043,.T.);
#3944=EDGE_CURVE('',#3284,#3290,#2044,.T.);
#3945=EDGE_CURVE('',#3274,#3285,#2045,.T.);
#5044=ORIENTED_EDGE('',*,*,#3907,.F.);
#5045=ORIENTED_EDGE('',*,*,#3908,.F.);
#5046=ORIENTED_EDGE('',*,*,#3909,.F.);
#5047=ORIENTED_EDGE('',*,*,#3910,.F.);
#5048=ORIENTED_EDGE('',*,*,#3909,.T.);
#5049=ORIENTED_EDGE('',*,*,#3911,.T.);
#5050=ORIENTED_EDGE('',*,*,#3912,.F.);
#5051=ORIENTED_EDGE('',*,*,#3913,.F.);
#5052=ORIENTED_EDGE('',*,*,#3914,.T.);
#5053=ORIENTED_EDGE('',*,*,#3915,.T.);
#5054=ORIENTED_EDGE('',*,*,#3916,.T.);
#5055=ORIENTED_EDGE('',*,*,#3912,.T.);
#5056=ORIENTED_EDGE('',*,*,#3917,.T.);
#5057=ORIENTED_EDGE('',*,*,#3914,.F.);
#5058=ORIENTED_EDGE('',*,*,#3911,.F.);
#5059=ORIENTED_EDGE('',*,*,#3908,.T.);
#5060=ORIENTED_EDGE('',*,*,#3918,.F.);
#5061=ORIENTED_EDGE('',*,*,#3919,.F.);
#5062=ORIENTED_EDGE('',*,*,#3920,.T.);
#5063=ORIENTED_EDGE('',*,*,#3921,.F.);
#5064=ORIENTED_EDGE('',*,*,#3922,.T.);
#5065=ORIENTED_EDGE('',*,*,#3923,.T.);
#5066=ORIENTED_EDGE('',*,*,#3924,.T.);
#5067=ORIENTED_EDGE('',*,*,#3925,.T.);
#5068=ORIENTED_EDGE('',*,*,#3926,.T.);
#5069=ORIENTED_EDGE('',*,*,#3915,.F.);
#5070=ORIENTED_EDGE('',*,*,#3924,.F.);
#5071=ORIENTED_EDGE('',*,*,#3927,.F.);
#5072=ORIENTED_EDGE('',*,*,#3928,.F.);
#5073=ORIENTED_EDGE('',*,*,#3925,.F.);
#5074=ORIENTED_EDGE('',*,*,#3923,.F.);
#5075=ORIENTED_EDGE('',*,*,#3916,.F.);
#5076=ORIENTED_EDGE('',*,*,#3926,.F.);
#5077=ORIENTED_EDGE('',*,*,#3928,.T.);
#5078=ORIENTED_EDGE('',*,*,#3929,.F.);
#5079=ORIENTED_EDGE('',*,*,#3930,.F.);
#5080=ORIENTED_EDGE('',*,*,#3931,.T.);
#5081=ORIENTED_EDGE('',*,*,#3932,.F.);
#5082=ORIENTED_EDGE('',*,*,#3933,.T.);
#5083=ORIENTED_EDGE('',*,*,#3910,.T.);
#5084=ORIENTED_EDGE('',*,*,#3913,.T.);
#5085=ORIENTED_EDGE('',*,*,#3927,.T.);
#5086=ORIENTED_EDGE('',*,*,#3922,.F.);
#5087=ORIENTED_EDGE('',*,*,#3934,.F.);
#5088=ORIENTED_EDGE('',*,*,#3929,.T.);
#5089=ORIENTED_EDGE('',*,*,#3930,.T.);
#5090=ORIENTED_EDGE('',*,*,#3934,.T.);
#5091=ORIENTED_EDGE('',*,*,#3921,.T.);
#5092=ORIENTED_EDGE('',*,*,#3935,.T.);
#5093=ORIENTED_EDGE('',*,*,#3936,.T.);
#5094=ORIENTED_EDGE('',*,*,#3937,.T.);
#5095=ORIENTED_EDGE('',*,*,#3936,.F.);
#5096=ORIENTED_EDGE('',*,*,#3938,.F.);
#5097=ORIENTED_EDGE('',*,*,#3939,.T.);
#5098=ORIENTED_EDGE('',*,*,#3917,.F.);
#5099=ORIENTED_EDGE('',*,*,#3939,.F.);
#5100=ORIENTED_EDGE('',*,*,#3940,.F.);
#5101=ORIENTED_EDGE('',*,*,#3941,.F.);
#5102=ORIENTED_EDGE('',*,*,#3942,.F.);
#5103=ORIENTED_EDGE('',*,*,#3935,.F.);
#5104=ORIENTED_EDGE('',*,*,#3920,.F.);
#5105=ORIENTED_EDGE('',*,*,#3943,.F.);
#5106=ORIENTED_EDGE('',*,*,#3940,.T.);
#5107=ORIENTED_EDGE('',*,*,#3938,.T.);
#5108=ORIENTED_EDGE('',*,*,#3937,.F.);
#5109=ORIENTED_EDGE('',*,*,#3942,.T.);
#5110=ORIENTED_EDGE('',*,*,#3944,.F.);
#5111=ORIENTED_EDGE('',*,*,#3931,.F.);
#5112=ORIENTED_EDGE('',*,*,#3919,.T.);
#5113=ORIENTED_EDGE('',*,*,#3945,.T.);
#5114=ORIENTED_EDGE('',*,*,#3932,.T.);
#5115=ORIENTED_EDGE('',*,*,#3944,.T.);
#5116=ORIENTED_EDGE('',*,*,#3941,.T.);
#5117=ORIENTED_EDGE('',*,*,#3943,.T.);
#5118=ORIENTED_EDGE('',*,*,#3907,.T.);
#5119=ORIENTED_EDGE('',*,*,#3933,.F.);
#5120=ORIENTED_EDGE('',*,*,#3945,.F.);
#5121=ORIENTED_EDGE('',*,*,#3918,.T.);
#5933=CYLINDRICAL_SURFACE('',#6980,0.2117);
#6131=ADVANCED_FACE('',(#1068),#787,.F.);
#6132=ADVANCED_FACE('',(#1069),#788,.T.);
#6133=ADVANCED_FACE('',(#1070,#612),#789,.T.);
#6134=ADVANCED_FACE('',(#1071),#790,.T.);
#6135=ADVANCED_FACE('',(#1072),#791,.T.);
#6136=ADVANCED_FACE('',(#1073),#792,.F.);
#6137=ADVANCED_FACE('',(#1074),#793,.T.);
#6138=ADVANCED_FACE('',(#1075),#794,.T.);
#6139=ADVANCED_FACE('',(#1076),#795,.T.);
#6140=ADVANCED_FACE('',(#1077),#5933,.F.);
#6141=ADVANCED_FACE('',(#1078),#796,.F.);
#6142=ADVANCED_FACE('',(#1079),#797,.F.);
#6143=ADVANCED_FACE('',(#1080),#798,.T.);
#6144=ADVANCED_FACE('',(#1081),#799,.T.);
#6340=CLOSED_SHELL('',(#6131,#6132,#6133,#6134,#6135,#6136,#6137,#6138,
#6139,#6140,#6141,#6142,#6143,#6144));
#6968=AXIS2_PLACEMENT_3D('',#9998,#8152,#8153);
#6969=AXIS2_PLACEMENT_3D('',#9999,#8154,#8155);
#6970=AXIS2_PLACEMENT_3D('',#10008,#8160,#8161);
#6971=AXIS2_PLACEMENT_3D('',#10014,#8165,#8166);
#6972=AXIS2_PLACEMENT_3D('',#10021,#8170,#8171);
#6973=AXIS2_PLACEMENT_3D('',#10022,#8172,#8173);
#6974=AXIS2_PLACEMENT_3D('',#10036,#8181,#8182);
#6975=AXIS2_PLACEMENT_3D('',#10040,#8185,#8186);
#6976=AXIS2_PLACEMENT_3D('',#10044,#8189,#8190);
#6977=AXIS2_PLACEMENT_3D('',#10054,#8196,#8197);
#6978=AXIS2_PLACEMENT_3D('',#10056,#8199,#8200);
#6979=AXIS2_PLACEMENT_3D('',#10060,#8202,#8203);
#6980=AXIS2_PLACEMENT_3D('',#10062,#8205,#8206);
#6981=AXIS2_PLACEMENT_3D('',#10064,#8207,#8208);
#6982=AXIS2_PLACEMENT_3D('',#10067,#8210,#8211);
#6983=AXIS2_PLACEMENT_3D('',#10069,#8212,#8213);
#6984=AXIS2_PLACEMENT_3D('',#10070,#8214,#8215);
#6985=AXIS2_PLACEMENT_3D('',#10071,#8216,#8217);
#6986=AXIS2_PLACEMENT_3D('',#10073,#8219,#8220);
#6987=AXIS2_PLACEMENT_3D('',#10075,#8222,#8223);
#6988=AXIS2_PLACEMENT_3D('',#10077,#8225,#8226);
#8152=DIRECTION('axis',(0.,0.,1.));
#8153=DIRECTION('refdir',(1.,0.,0.));
#8154=DIRECTION('center_axis',(0.,0.,1.));
#8155=DIRECTION('ref_axis',(1.,0.,0.));
#8156=DIRECTION('',(1.,0.,0.));
#8157=DIRECTION('',(0.,-1.,0.));
#8158=DIRECTION('',(-1.,0.,0.));
#8159=DIRECTION('',(0.,1.,0.));
#8160=DIRECTION('center_axis',(0.,1.,0.));
#8161=DIRECTION('ref_axis',(-1.,0.,0.));
#8162=DIRECTION('',(0.,0.,1.));
#8163=DIRECTION('',(-1.,0.,0.));
#8164=DIRECTION('',(0.,0.,1.));
#8165=DIRECTION('center_axis',(0.,0.,1.));
#8166=DIRECTION('ref_axis',(1.,0.,0.));
#8167=DIRECTION('',(0.,-1.,0.));
#8168=DIRECTION('',(1.,0.,0.));
#8169=DIRECTION('',(0.,1.,0.));
#8170=DIRECTION('center_axis',(0.,0.,-1.));
#8171=DIRECTION('ref_axis',(1.,0.,0.));
#8172=DIRECTION('center_axis',(-1.,0.,0.));
#8173=DIRECTION('ref_axis',(0.,-1.,0.));
#8174=DIRECTION('',(0.,0.,1.));
#8175=DIRECTION('',(0.,0.707106781186548,0.707106781186548));
#8176=DIRECTION('',(0.,-1.,0.));
#8177=DIRECTION('',(0.,0.707106781186548,-0.707106781186548));
#8178=DIRECTION('',(0.,0.,1.));
#8179=DIRECTION('',(0.,-1.,0.));
#8180=DIRECTION('',(0.,0.,1.));
#8181=DIRECTION('center_axis',(0.,-1.,0.));
#8182=DIRECTION('ref_axis',(1.,0.,0.));
#8183=DIRECTION('',(1.,0.,0.));
#8184=DIRECTION('',(0.,0.,1.));
#8185=DIRECTION('center_axis',(0.,0.,1.));
#8186=DIRECTION('ref_axis',(1.,0.,0.));
#8187=DIRECTION('',(-1.,0.,0.));
#8188=DIRECTION('',(0.,1.,0.));
#8189=DIRECTION('center_axis',(1.,0.,0.));
#8190=DIRECTION('ref_axis',(0.,1.,0.));
#8191=DIRECTION('',(0.,0.,1.));
#8192=DIRECTION('',(0.,-0.707106781186548,0.707106781186548));
#8193=DIRECTION('',(0.,1.,0.));
#8194=DIRECTION('',(0.,-0.707106781186548,-0.707106781186548));
#8195=DIRECTION('',(0.,0.,1.));
#8196=DIRECTION('center_axis',(0.,-1.,0.));
#8197=DIRECTION('ref_axis',(1.,0.,0.));
#8198=DIRECTION('',(-1.,0.,0.));
#8199=DIRECTION('center_axis',(0.,-0.707106781186548,-0.707106781186548));
#8200=DIRECTION('ref_axis',(-1.,0.,0.));
#8201=DIRECTION('',(1.,0.,0.));
#8202=DIRECTION('center_axis',(0.,0.707106781186548,0.707106781186548));
#8203=DIRECTION('ref_axis',(0.,0.707106781186547,-0.707106781186547));
#8204=DIRECTION('',(1.,0.,0.));
#8205=DIRECTION('center_axis',(0.,0.,1.));
#8206=DIRECTION('ref_axis',(1.,0.,0.));
#8207=DIRECTION('center_axis',(0.,0.,-1.));
#8208=DIRECTION('ref_axis',(1.,0.,0.));
#8209=DIRECTION('',(0.,0.,1.));
#8210=DIRECTION('center_axis',(0.,0.,-1.));
#8211=DIRECTION('ref_axis',(1.,0.,0.));
#8212=DIRECTION('center_axis',(0.,-0.707106781186548,0.707106781186548));
#8213=DIRECTION('ref_axis',(0.,0.707106781186547,0.707106781186547));
#8214=DIRECTION('center_axis',(0.,0.,-1.));
#8215=DIRECTION('ref_axis',(1.,0.,0.));
#8216=DIRECTION('center_axis',(0.,0.,1.));
#8217=DIRECTION('ref_axis',(1.,0.,0.));
#8218=DIRECTION('',(-1.,0.,0.));
#8219=DIRECTION('center_axis',(0.,0.,1.));
#8220=DIRECTION('ref_axis',(1.,0.,0.));
#8221=DIRECTION('',(-1.,0.,0.));
#8222=DIRECTION('center_axis',(0.,0.707106781186548,-0.707106781186548));
#8223=DIRECTION('ref_axis',(-1.,0.,0.));
#8224=DIRECTION('',(1.,0.,0.));
#8225=DIRECTION('center_axis',(0.,1.,0.));
#8226=DIRECTION('ref_axis',(-1.,0.,0.));
#9998=CARTESIAN_POINT('',(0.,0.,0.));
#9999=CARTESIAN_POINT('Origin',(0.,0.395,0.25));
#10000=CARTESIAN_POINT('',(-0.5,0.3,0.25));
#10001=CARTESIAN_POINT('',(0.5,0.3,0.25));
#10002=CARTESIAN_POINT('',(0.25,0.3,0.25));
#10003=CARTESIAN_POINT('',(-0.5,0.5,0.25));
#10004=CARTESIAN_POINT('',(-0.5,0.5,0.25));
#10005=CARTESIAN_POINT('',(0.5,0.5,0.25));
#10006=CARTESIAN_POINT('',(0.5,0.5,0.25));
#10007=CARTESIAN_POINT('',(0.5,0.29,0.25));
#10008=CARTESIAN_POINT('Origin',(0.5,0.5,0.25));
#10009=CARTESIAN_POINT('',(-0.5,0.5,0.4));
#10010=CARTESIAN_POINT('',(-0.5,0.5,0.25));
#10011=CARTESIAN_POINT('',(0.5,0.5,0.4));
#10012=CARTESIAN_POINT('',(0.5,0.5,0.4));
#10013=CARTESIAN_POINT('',(0.5,0.5,0.25));
#10014=CARTESIAN_POINT('Origin',(0.,0.,0.4));
#10015=CARTESIAN_POINT('',(-0.5,-0.5,0.4));
#10016=CARTESIAN_POINT('',(-0.5,0.5,0.4));
#10017=CARTESIAN_POINT('',(0.5,-0.5,0.4));
#10018=CARTESIAN_POINT('',(-0.5,-0.5,0.4));
#10019=CARTESIAN_POINT('',(0.5,-0.3,0.4));
#10020=CARTESIAN_POINT('',(-0.2117,2.59257727379495E-17,0.4));
#10021=CARTESIAN_POINT('Origin',(0.,0.,0.4));
#10022=CARTESIAN_POINT('Origin',(-0.5,0.3,0.));
#10023=CARTESIAN_POINT('',(-0.5,0.3,0.15));
#10024=CARTESIAN_POINT('',(-0.5,0.3,0.));
#10025=CARTESIAN_POINT('',(-0.5,0.15,0.));
#10026=CARTESIAN_POINT('',(-0.5,0.225,0.075));
#10027=CARTESIAN_POINT('',(-0.5,-0.15,0.));
#10028=CARTESIAN_POINT('',(-0.5,0.3,0.));
#10029=CARTESIAN_POINT('',(-0.5,-0.3,0.15));
#10030=CARTESIAN_POINT('',(-0.5,-0.075,-0.075));
#10031=CARTESIAN_POINT('',(-0.5,-0.3,0.25));
#10032=CARTESIAN_POINT('',(-0.5,-0.3,0.));
#10033=CARTESIAN_POINT('',(-0.5,-0.5,0.25));
#10034=CARTESIAN_POINT('',(-0.5,-0.29,0.25));
#10035=CARTESIAN_POINT('',(-0.5,-0.5,0.25));
#10036=CARTESIAN_POINT('Origin',(-0.5,-0.5,0.25));
#10037=CARTESIAN_POINT('',(0.5,-0.5,0.25));
#10038=CARTESIAN_POINT('',(-0.5,-0.5,0.25));
#10039=CARTESIAN_POINT('',(0.5,-0.5,0.25));
#10040=CARTESIAN_POINT('Origin',(0.,-0.395,0.25));
#10041=CARTESIAN_POINT('',(0.5,-0.3,0.25));
#10042=CARTESIAN_POINT('',(-0.25,-0.3,0.25));
#10043=CARTESIAN_POINT('',(0.5,-0.5,0.25));
#10044=CARTESIAN_POINT('Origin',(0.5,-0.3,0.));
#10045=CARTESIAN_POINT('',(0.5,-0.3,0.15));
#10046=CARTESIAN_POINT('',(0.5,-0.3,0.));
#10047=CARTESIAN_POINT('',(0.5,-0.15,0.));
#10048=CARTESIAN_POINT('',(0.5,-0.225,0.075));
#10049=CARTESIAN_POINT('',(0.5,0.15,0.));
#10050=CARTESIAN_POINT('',(0.5,-0.3,0.));
#10051=CARTESIAN_POINT('',(0.5,0.3,0.15));
#10052=CARTESIAN_POINT('',(0.5,0.075,-0.075));
#10053=CARTESIAN_POINT('',(0.5,0.3,0.));
#10054=CARTESIAN_POINT('Origin',(-0.5,-0.3,0.));
#10055=CARTESIAN_POINT('',(-0.25,-0.3,0.15));
#10056=CARTESIAN_POINT('Origin',(-0.25,-0.225,0.075));
#10057=CARTESIAN_POINT('',(-0.149388386429468,-0.15,0.));
#10058=CARTESIAN_POINT('',(-0.25,-0.15,0.));
#10059=CARTESIAN_POINT('',(0.149388386429468,-0.15,0.));
#10060=CARTESIAN_POINT('Origin',(0.,0.,-0.15));
#10061=CARTESIAN_POINT('',(-0.25,-0.15,0.));
#10062=CARTESIAN_POINT('Origin',(0.,0.,-0.1));
#10063=CARTESIAN_POINT('',(-0.2117,-2.59257727379495E-17,0.));
#10064=CARTESIAN_POINT('Origin',(0.,0.,0.));
#10065=CARTESIAN_POINT('',(-0.2117,-2.59257727379495E-17,-0.1));
#10066=CARTESIAN_POINT('',(-0.149388386429468,0.15,0.));
#10067=CARTESIAN_POINT('Origin',(0.,0.,0.));
#10068=CARTESIAN_POINT('',(0.149388386429468,0.15,0.));
#10069=CARTESIAN_POINT('Origin',(0.,0.,-0.15));
#10070=CARTESIAN_POINT('Origin',(0.,0.,0.));
#10071=CARTESIAN_POINT('Origin',(0.,0.,0.));
#10072=CARTESIAN_POINT('',(0.25,0.15,0.));
#10073=CARTESIAN_POINT('Origin',(0.,0.,0.));
#10074=CARTESIAN_POINT('',(0.25,0.15,0.));
#10075=CARTESIAN_POINT('Origin',(0.25,0.225,0.075));
#10076=CARTESIAN_POINT('',(0.25,0.3,0.15));
#10077=CARTESIAN_POINT('Origin',(0.5,0.3,0.));
#11504=UNCERTAINTY_MEASURE_WITH_UNIT(LENGTH_MEASURE(0.001),#11560,
'DISTANCE_ACCURACY_VALUE',
'Maximum model space distance between geometric entities at asserted c
onnectivities');
#11522=UNCERTAINTY_MEASURE_WITH_UNIT(LENGTH_MEASURE(0.001),#11560,
'DISTANCE_ACCURACY_VALUE',
'Maximum model space distance between geometric entities at asserted c
onnectivities');
#11541=(
GEOMETRIC_REPRESENTATION_CONTEXT(3)
GLOBAL_UNCERTAINTY_ASSIGNED_CONTEXT((#11504))
GLOBAL_UNIT_ASSIGNED_CONTEXT((#11560,#11562,#11563))
REPRESENTATION_CONTEXT('','3D')
);
#11559=(
GEOMETRIC_REPRESENTATION_CONTEXT(3)
GLOBAL_UNCERTAINTY_ASSIGNED_CONTEXT((#11522))
GLOBAL_UNIT_ASSIGNED_CONTEXT((#11560,#11562,#11563))
REPRESENTATION_CONTEXT('','3D')
);
#11560=(
LENGTH_UNIT()
NAMED_UNIT(*)
SI_UNIT(.CENTI.,.METRE.)
);
#11562=(
NAMED_UNIT(*)
PLANE_ANGLE_UNIT()
SI_UNIT($,.RADIAN.)
);
#11563=(
NAMED_UNIT(*)
SI_UNIT($,.STERADIAN.)
SOLID_ANGLE_UNIT()
);
#11582=SHAPE_DEFINITION_REPRESENTATION(#11618,#11739);
#11618=PRODUCT_DEFINITION_SHAPE('',$,#11776);
#11739=SHAPE_REPRESENTATION('',(#6968),#11541);
#11757=PRODUCT_DEFINITION_CONTEXT('part definition',#11867,'design');
#11776=PRODUCT_DEFINITION('Captive slot nut','Captive slot nut',#11812,
#11757);
#11812=PRODUCT_DEFINITION_FORMATION('',$,#11887);
#11867=APPLICATION_CONTEXT(
'Core Data for Automotive Mechanical Design Process');
#11868=PRODUCT_CONTEXT('part definition',#11867,'mechanical');
#11887=PRODUCT('Captive slot nut','Captive slot nut','Captive slot nut',
(#11868));
#11968=COLOUR_RGB('Black',0.12,0.14,0.17);
#11969=FILL_AREA_STYLE_COLOUR('',#11968);
#11970=FILL_AREA_STYLE('',(#11969));
#11971=SURFACE_STYLE_FILL_AREA(#11970);
#11972=SURFACE_SIDE_STYLE('',(#11971));
#11973=SURFACE_STYLE_USAGE(.BOTH.,#11972);
#11974=PRESENTATION_STYLE_ASSIGNMENT((#11973));
ENDSEC;
END-ISO-10303-21;
